ISO-10303-21;
HEADER;
/* Generated by software containing ST-Developer
 * from STEP Tools, Inc. (www.steptools.com) 
 */

FILE_DESCRIPTION(
/* description */ ('XY cross-slide table'),
/* implementation_level */ '2;1');

FILE_NAME(
/* name */ 'Flat Washer - M6 (1).step',
/* time_stamp */ '2026-10-28T03:22:46-07:00',
/* author */ (''),
/* organization */ (''),
/* preprocessor_version */ 'ST-DEVELOPER v20.2',
/* originating_system */ 'Autodesk Translation Framework v15.17.0.0',
/* authorisation */ '');

FILE_SCHEMA (('AUTOMOTIVE_DESIGN { 1 0 10303 214 3 1 1 }'));
ENDSEC;

DATA;
#10=MECHANICAL_DESIGN_GEOMETRIC_PRESENTATION_REPRESENTATION('',(#1781),#62984);
#1585=SHAPE_REPRESENTATION_RELATIONSHIP('SRR','None',#63445,#1668);
#1668=ADVANCED_BREP_SHAPE_REPRESENTATION('',(#1886),#62982);
#1781=STYLED_ITEM('',(#63919),#1886);
#1886=MANIFOLD_SOLID_BREP('Body1',#23083);
#2293=FACE_BOUND('',#5885,.T.);
#2294=FACE_BOUND('',#5887,.T.);
#2856=PLANE('',#26382);
#2857=PLANE('',#26383);
#4162=FACE_OUTER_BOUND('',#5882,.T.);
#4163=FACE_OUTER_BOUND('',#5883,.T.);
#4164=FACE_OUTER_BOUND('',#5884,.T.);
#4165=FACE_OUTER_BOUND('',#5886,.T.);
#5882=EDGE_LOOP('',(#20964,#20965,#20966,#20967));
#5883=EDGE_LOOP('',(#20968,#20969,#20970,#20971));
#5884=EDGE_LOOP('',(#20972));
#5885=EDGE_LOOP('',(#20973));
#5886=EDGE_LOOP('',(#20974));
#5887=EDGE_LOOP('',(#20975));
#7367=LINE('',#62656,#8854);
#7368=LINE('',#62662,#8855);
#8854=VECTOR('',#32678,0.32);
#8855=VECTOR('',#32685,0.6);
#9761=CIRCLE('',#26377,0.32);
#9762=CIRCLE('',#26378,0.32);
#9763=CIRCLE('',#26380,0.6);
#9764=CIRCLE('',#26381,0.6);
#11812=VERTEX_POINT('',#62653);
#11813=VERTEX_POINT('',#62655);
#11814=VERTEX_POINT('',#62659);
#11815=VERTEX_POINT('',#62661);
#14866=EDGE_CURVE('',#11812,#11812,#9761,.T.);
#14867=EDGE_CURVE('',#11812,#11813,#7367,.T.);
#14868=EDGE_CURVE('',#11813,#11813,#9762,.T.);
#14869=EDGE_CURVE('',#11814,#11814,#9763,.T.);
#14870=EDGE_CURVE('',#11814,#11815,#7368,.T.);
#14871=EDGE_CURVE('',#11815,#11815,#9764,.T.);
#20964=ORIENTED_EDGE('',*,*,#14866,.F.);
#20965=ORIENTED_EDGE('',*,*,#14867,.T.);
#20966=ORIENTED_EDGE('',*,*,#14868,.T.);
#20967=ORIENTED_EDGE('',*,*,#14867,.F.);
#20968=ORIENTED_EDGE('',*,*,#14869,.F.);
#20969=ORIENTED_EDGE('',*,*,#14870,.T.);
#20970=ORIENTED_EDGE('',*,*,#14871,.T.);
#20971=ORIENTED_EDGE('',*,*,#14870,.F.);
#20972=ORIENTED_EDGE('',*,*,#14869,.T.);
#20973=ORIENTED_EDGE('',*,*,#14866,.T.);
#20974=ORIENTED_EDGE('',*,*,#14871,.F.);
#20975=ORIENTED_EDGE('',*,*,#14868,.F.);
#21646=CYLINDRICAL_SURFACE('',#26376,0.32);
#21647=CYLINDRICAL_SURFACE('',#26379,0.6);
#22943=ADVANCED_FACE('',(#4162),#21646,.F.);
#22944=ADVANCED_FACE('',(#4163),#21647,.T.);
#22945=ADVANCED_FACE('',(#4164,#2293),#2856,.T.);
#22946=ADVANCED_FACE('',(#4165,#2294),#2857,.F.);
#23083=CLOSED_SHELL('',(#22943,#22944,#22945,#22946));
#26375=AXIS2_PLACEMENT_3D('',#62651,#32672,#32673);
#26376=AXIS2_PLACEMENT_3D('',#62652,#32674,#32675);
#26377=AXIS2_PLACEMENT_3D('',#62654,#32676,#32677);
#26378=AXIS2_PLACEMENT_3D('',#62657,#32679,#32680);
#26379=AXIS2_PLACEMENT_3D('',#62658,#32681,#32682);
#26380=AXIS2_PLACEMENT_3D('',#62660,#32683,#32684);
#26381=AXIS2_PLACEMENT_3D('',#62663,#32686,#32687);
#26382=AXIS2_PLACEMENT_3D('',#62664,#32688,#32689);
#26383=AXIS2_PLACEMENT_3D('',#62665,#32690,#32691);
#32672=DIRECTION('axis',(0.,0.,1.));
#32673=DIRECTION('refdir',(1.,0.,0.));
#32674=DIRECTION('center_axis',(0.,1.,0.));
#32675=DIRECTION('ref_axis',(1.,0.,0.));
#32676=DIRECTION('center_axis',(0.,-1.,0.));
#32677=DIRECTION('ref_axis',(1.,0.,0.));
#32678=DIRECTION('',(0.,-1.,0.));
#32679=DIRECTION('center_axis',(0.,-1.,0.));
#32680=DIRECTION('ref_axis',(1.,0.,0.));
#32681=DIRECTION('center_axis',(0.,1.,0.));
#32682=DIRECTION('ref_axis',(1.,0.,0.));
#32683=DIRECTION('center_axis',(0.,1.,0.));
#32684=DIRECTION('ref_axis',(1.,0.,0.));
#32685=DIRECTION('',(0.,-1.,0.));
#32686=DIRECTION('center_axis',(0.,1.,0.));
#32687=DIRECTION('ref_axis',(1.,0.,0.));
#32688=DIRECTION('center_axis',(0.,1.,0.));
#32689=DIRECTION('ref_axis',(1.,0.,0.));
#32690=DIRECTION('center_axis',(0.,1.,0.));
#32691=DIRECTION('ref_axis',(1.,0.,0.));
#62651=CARTESIAN_POINT('',(0.,0.,0.));
#62652=CARTESIAN_POINT('Origin',(0.,0.,0.));
#62653=CARTESIAN_POINT('',(-0.32,0.16,3.91886975727153E-17));
#62654=CARTESIAN_POINT('Origin',(0.,0.16,0.));
#62655=CARTESIAN_POINT('',(-0.32,0.,3.91886975727153E-17));
#62656=CARTESIAN_POINT('',(-0.32,0.,3.91886975727153E-17));
#62657=CARTESIAN_POINT('Origin',(0.,0.,0.));
#62658=CARTESIAN_POINT('Origin',(0.,0.,0.));
#62659=CARTESIAN_POINT('',(-0.6,0.16,7.34788079488412E-17));
#62660=CARTESIAN_POINT('Origin',(0.,0.16,0.));
#62661=CARTESIAN_POINT('',(-0.6,0.,7.34788079488412E-17));
#62662=CARTESIAN_POINT('',(-0.6,0.,7.34788079488412E-17));
#62663=CARTESIAN_POINT('Origin',(0.,0.,0.));
#62664=CARTESIAN_POINT('Origin',(0.,0.16,0.));
#62665=CARTESIAN_POINT('Origin',(0.,0.,0.));
#62883=UNCERTAINTY_MEASURE_WITH_UNIT(LENGTH_MEASURE(0.001),#62985,
'DISTANCE_ACCURACY_VALUE',
'Maximum model space distance between geometric entities at asserted c
onnectivities');
#62885=UNCERTAINTY_MEASURE_WITH_UNIT(LENGTH_MEASURE(0.001),#62985,
'DISTANCE_ACCURACY_VALUE',
'Maximum model space distance between geometric entities at asserted c
onnectivities');
#62982=(
GEOMETRIC_REPRESENTATION_CONTEXT(3)
GLOBAL_UNCERTAINTY_ASSIGNED_CONTEXT((#62883))
GLOBAL_UNIT_ASSIGNED_CONTEXT((#62985,#62987,#62988))
REPRESENTATION_CONTEXT('','3D')
);
#62984=(
GEOMETRIC_REPRESENTATION_CONTEXT(3)
GLOBAL_UNCERTAINTY_ASSIGNED_CONTEXT((#62885))
GLOBAL_UNIT_ASSIGNED_CONTEXT((#62985,#62987,#62988))
REPRESENTATION_CONTEXT('','3D')
);
#62985=(
LENGTH_UNIT()
NAMED_UNIT(*)
SI_UNIT(.CENTI.,.METRE.)
);
#62987=(
NAMED_UNIT(*)
PLANE_ANGLE_UNIT()
SI_UNIT($,.RADIAN.)
);
#62988=(
NAMED_UNIT(*)
SI_UNIT($,.STERADIAN.)
SOLID_ANGLE_UNIT()
);
#63085=SHAPE_DEFINITION_REPRESENTATION(#63296,#63445);
#63296=PRODUCT_DEFINITION_SHAPE('',$,#63544);
#63445=SHAPE_REPRESENTATION('',(#26375),#62982);
#63447=PRODUCT_DEFINITION_CONTEXT('part definition',#63743,'design');
#63544=PRODUCT_DEFINITION('Flat Washer - M6 (1)','Flat Washer - M6 (1)',#63642,
#63447);
#63642=PRODUCT_DEFINITION_FORMATION('',$,#63841);
#63743=APPLICATION_CONTEXT(
'Core Data for Automotive Mechanical Design Process');
#63744=PRODUCT_CONTEXT('part definition',#63743,'mechanical');
#63841=PRODUCT('Flat Washer - M6 (1)','Flat Washer - M6 (1)',
'Flat Washer - M6 (1)',(#63744));
#63913=COLOUR_RGB('Black',0.12,0.14,0.17);
#63914=FILL_AREA_STYLE_COLOUR('',#63913);
#63915=FILL_AREA_STYLE('',(#63914));
#63916=SURFACE_STYLE_FILL_AREA(#63915);
#63917=SURFACE_SIDE_STYLE('',(#63916));
#63918=SURFACE_STYLE_USAGE(.BOTH.,#63917);
#63919=PRESENTATION_STYLE_ASSIGNMENT((#63918));
ENDSEC;
END-ISO-10303-21;
